ISO-10303-21;
HEADER;
/* Generated by software containing ST-Developer
 * from STEP Tools, Inc. (www.steptools.com) 
 */

FILE_DESCRIPTION(
/* description */ ('PAT-080'),
/* implementation_level */ '2;1');

FILE_NAME(
/* name */ 'Pipe section (1).step',
/* time_stamp */ '2026-10-29T20:13:47-07:00',
/* author */ (''),
/* organization */ (''),
/* preprocessor_version */ 'ST-DEVELOPER v20.2',
/* originating_system */ 'Autodesk Translation Framework v15.17.0.0',
/* authorisation */ '');

FILE_SCHEMA (('AUTOMOTIVE_DESIGN { 1 0 10303 214 3 1 1 }'));
ENDSEC;

DATA;
#10=MECHANICAL_DESIGN_GEOMETRIC_PRESENTATION_REPRESENTATION('',(#255),#6878);
#217=SHAPE_REPRESENTATION_RELATIONSHIP('SRR','None',#6973,#236);
#236=ADVANCED_BREP_SHAPE_REPRESENTATION('',(#274),#6868);
#255=STYLED_ITEM('',(#7122),#274);
#274=MANIFOLD_SOLID_BREP('Body1',#3871);
#323=FACE_BOUND('',#880,.T.);
#324=FACE_BOUND('',#884,.T.);
#325=FACE_BOUND('',#886,.T.);
#433=PLANE('',#4286);
#434=PLANE('',#4293);
#435=PLANE('',#4294);
#610=FACE_OUTER_BOUND('',#878,.T.);
#611=FACE_OUTER_BOUND('',#879,.T.);
#612=FACE_OUTER_BOUND('',#881,.T.);
#613=FACE_OUTER_BOUND('',#882,.T.);
#614=FACE_OUTER_BOUND('',#883,.T.);
#615=FACE_OUTER_BOUND('',#885,.T.);
#878=EDGE_LOOP('',(#3124,#3125,#3126,#3127));
#879=EDGE_LOOP('',(#3128));
#880=EDGE_LOOP('',(#3129));
#881=EDGE_LOOP('',(#3130,#3131,#3132,#3133));
#882=EDGE_LOOP('',(#3134,#3135,#3136,#3137));
#883=EDGE_LOOP('',(#3138));
#884=EDGE_LOOP('',(#3139));
#885=EDGE_LOOP('',(#3140));
#886=EDGE_LOOP('',(#3141));
#1218=LINE('',#6284,#1533);
#1219=LINE('',#6291,#1534);
#1220=LINE('',#6297,#1535);
#1533=VECTOR('',#5106,0.93);
#1534=VECTOR('',#5115,0.79);
#1535=VECTOR('',#5122,1.3);
#1726=CIRCLE('',#4284,0.93);
#1727=CIRCLE('',#4285,0.93);
#1728=CIRCLE('',#4287,0.79);
#1729=CIRCLE('',#4289,0.79);
#1730=CIRCLE('',#4291,1.3);
#1731=CIRCLE('',#4292,1.3);
#1982=VERTEX_POINT('',#6281);
#1983=VERTEX_POINT('',#6283);
#1984=VERTEX_POINT('',#6287);
#1985=VERTEX_POINT('',#6290);
#1986=VERTEX_POINT('',#6294);
#1987=VERTEX_POINT('',#6296);
#2385=EDGE_CURVE('',#1982,#1982,#1726,.T.);
#2386=EDGE_CURVE('',#1982,#1983,#1218,.T.);
#2387=EDGE_CURVE('',#1983,#1983,#1727,.T.);
#2388=EDGE_CURVE('',#1984,#1984,#1728,.T.);
#2389=EDGE_CURVE('',#1984,#1985,#1219,.T.);
#2390=EDGE_CURVE('',#1985,#1985,#1729,.T.);
#2391=EDGE_CURVE('',#1986,#1986,#1730,.T.);
#2392=EDGE_CURVE('',#1986,#1987,#1220,.T.);
#2393=EDGE_CURVE('',#1987,#1987,#1731,.T.);
#3124=ORIENTED_EDGE('',*,*,#2385,.F.);
#3125=ORIENTED_EDGE('',*,*,#2386,.T.);
#3126=ORIENTED_EDGE('',*,*,#2387,.F.);
#3127=ORIENTED_EDGE('',*,*,#2386,.F.);
#3128=ORIENTED_EDGE('',*,*,#2385,.T.);
#3129=ORIENTED_EDGE('',*,*,#2388,.F.);
#3130=ORIENTED_EDGE('',*,*,#2388,.T.);
#3131=ORIENTED_EDGE('',*,*,#2389,.T.);
#3132=ORIENTED_EDGE('',*,*,#2390,.T.);
#3133=ORIENTED_EDGE('',*,*,#2389,.F.);
#3134=ORIENTED_EDGE('',*,*,#2391,.F.);
#3135=ORIENTED_EDGE('',*,*,#2392,.T.);
#3136=ORIENTED_EDGE('',*,*,#2393,.T.);
#3137=ORIENTED_EDGE('',*,*,#2392,.F.);
#3138=ORIENTED_EDGE('',*,*,#2391,.T.);
#3139=ORIENTED_EDGE('',*,*,#2387,.T.);
#3140=ORIENTED_EDGE('',*,*,#2393,.F.);
#3141=ORIENTED_EDGE('',*,*,#2390,.F.);
#3604=CYLINDRICAL_SURFACE('',#4283,0.93);
#3605=CYLINDRICAL_SURFACE('',#4288,0.79);
#3606=CYLINDRICAL_SURFACE('',#4290,1.3);
#3746=ADVANCED_FACE('',(#610),#3604,.F.);
#3747=ADVANCED_FACE('',(#611,#323),#433,.T.);
#3748=ADVANCED_FACE('',(#612),#3605,.F.);
#3749=ADVANCED_FACE('',(#613),#3606,.T.);
#3750=ADVANCED_FACE('',(#614,#324),#434,.T.);
#3751=ADVANCED_FACE('',(#615,#325),#435,.F.);
#3871=CLOSED_SHELL('',(#3746,#3747,#3748,#3749,#3750,#3751));
#4282=AXIS2_PLACEMENT_3D('',#6279,#5100,#5101);
#4283=AXIS2_PLACEMENT_3D('',#6280,#5102,#5103);
#4284=AXIS2_PLACEMENT_3D('',#6282,#5104,#5105);
#4285=AXIS2_PLACEMENT_3D('',#6285,#5107,#5108);
#4286=AXIS2_PLACEMENT_3D('',#6286,#5109,#5110);
#4287=AXIS2_PLACEMENT_3D('',#6288,#5111,#5112);
#4288=AXIS2_PLACEMENT_3D('',#6289,#5113,#5114);
#4289=AXIS2_PLACEMENT_3D('',#6292,#5116,#5117);
#4290=AXIS2_PLACEMENT_3D('',#6293,#5118,#5119);
#4291=AXIS2_PLACEMENT_3D('',#6295,#5120,#5121);
#4292=AXIS2_PLACEMENT_3D('',#6298,#5123,#5124);
#4293=AXIS2_PLACEMENT_3D('',#6299,#5125,#5126);
#4294=AXIS2_PLACEMENT_3D('',#6300,#5127,#5128);
#5100=DIRECTION('axis',(0.,0.,1.));
#5101=DIRECTION('refdir',(1.,0.,0.));
#5102=DIRECTION('center_axis',(1.,0.,0.));
#5103=DIRECTION('ref_axis',(0.,0.,-1.));
#5104=DIRECTION('center_axis',(1.,0.,0.));
#5105=DIRECTION('ref_axis',(0.,0.,-1.));
#5106=DIRECTION('',(1.,0.,0.));
#5107=DIRECTION('center_axis',(-1.,0.,0.));
#5108=DIRECTION('ref_axis',(0.,0.,-1.));
#5109=DIRECTION('center_axis',(1.,0.,0.));
#5110=DIRECTION('ref_axis',(0.,0.,-1.));
#5111=DIRECTION('center_axis',(1.,0.,0.));
#5112=DIRECTION('ref_axis',(0.,0.,-1.));
#5113=DIRECTION('center_axis',(1.,0.,0.));
#5114=DIRECTION('ref_axis',(0.,0.,-1.));
#5115=DIRECTION('',(-1.,0.,0.));
#5116=DIRECTION('center_axis',(-1.,0.,0.));
#5117=DIRECTION('ref_axis',(0.,0.,-1.));
#5118=DIRECTION('center_axis',(1.,0.,0.));
#5119=DIRECTION('ref_axis',(0.,0.,-1.));
#5120=DIRECTION('center_axis',(1.,0.,0.));
#5121=DIRECTION('ref_axis',(0.,0.,-1.));
#5122=DIRECTION('',(-1.,0.,0.));
#5123=DIRECTION('center_axis',(1.,0.,0.));
#5124=DIRECTION('ref_axis',(0.,0.,-1.));
#5125=DIRECTION('center_axis',(1.,0.,0.));
#5126=DIRECTION('ref_axis',(0.,0.,-1.));
#5127=DIRECTION('center_axis',(1.,0.,0.));
#5128=DIRECTION('ref_axis',(0.,0.,-1.));
#6279=CARTESIAN_POINT('',(0.,0.,0.));
#6280=CARTESIAN_POINT('Origin',(5.45,0.,6.));
#6281=CARTESIAN_POINT('',(5.45,-1.13892152320704E-16,6.93));
#6282=CARTESIAN_POINT('Origin',(5.45,0.,6.));
#6283=CARTESIAN_POINT('',(6.8,1.13892152320704E-16,6.93));
#6284=CARTESIAN_POINT('',(5.45,-1.13892152320704E-16,6.93));
#6285=CARTESIAN_POINT('Origin',(6.8,0.,6.));
#6286=CARTESIAN_POINT('Origin',(5.45,0.,6.));
#6287=CARTESIAN_POINT('',(5.45,-9.67470971326409E-17,6.79));
#6288=CARTESIAN_POINT('Origin',(5.45,0.,6.));
#6289=CARTESIAN_POINT('Origin',(2.8,0.,6.));
#6290=CARTESIAN_POINT('',(2.8,-9.67470971326409E-17,6.79));
#6291=CARTESIAN_POINT('',(2.8,-9.67470971326409E-17,6.79));
#6292=CARTESIAN_POINT('Origin',(2.8,0.,6.));
#6293=CARTESIAN_POINT('Origin',(2.8,0.,6.));
#6294=CARTESIAN_POINT('',(6.8,-1.59204083889156E-16,7.3));
#6295=CARTESIAN_POINT('Origin',(6.8,0.,6.));
#6296=CARTESIAN_POINT('',(2.8,-1.59204083889156E-16,7.3));
#6297=CARTESIAN_POINT('',(2.8,-1.59204083889156E-16,7.3));
#6298=CARTESIAN_POINT('Origin',(2.8,0.,6.));
#6299=CARTESIAN_POINT('Origin',(6.8,0.,6.));
#6300=CARTESIAN_POINT('Origin',(2.8,0.,6.));
#6847=UNCERTAINTY_MEASURE_WITH_UNIT(LENGTH_MEASURE(0.001),#6879,
'DISTANCE_ACCURACY_VALUE',
'Maximum model space distance between geometric entities at asserted c
onnectivities');
#6857=UNCERTAINTY_MEASURE_WITH_UNIT(LENGTH_MEASURE(0.001),#6879,
'DISTANCE_ACCURACY_VALUE',
'Maximum model space distance between geometric entities at asserted c
onnectivities');
#6868=(
GEOMETRIC_REPRESENTATION_CONTEXT(3)
GLOBAL_UNCERTAINTY_ASSIGNED_CONTEXT((#6847))
GLOBAL_UNIT_ASSIGNED_CONTEXT((#6879,#6881,#6882))
REPRESENTATION_CONTEXT('','3D')
);
#6878=(
GEOMETRIC_REPRESENTATION_CONTEXT(3)
GLOBAL_UNCERTAINTY_ASSIGNED_CONTEXT((#6857))
GLOBAL_UNIT_ASSIGNED_CONTEXT((#6879,#6881,#6882))
REPRESENTATION_CONTEXT('','3D')
);
#6879=(
LENGTH_UNIT()
NAMED_UNIT(*)
SI_UNIT(.CENTI.,.METRE.)
);
#6881=(
NAMED_UNIT(*)
PLANE_ANGLE_UNIT()
SI_UNIT($,.RADIAN.)
);
#6882=(
NAMED_UNIT(*)
SI_UNIT($,.STERADIAN.)
SOLID_ANGLE_UNIT()
);
#6893=SHAPE_DEFINITION_REPRESENTATION(#6913,#6973);
#6913=PRODUCT_DEFINITION_SHAPE('',$,#6994);
#6973=SHAPE_REPRESENTATION('',(#4282),#6868);
#6983=PRODUCT_DEFINITION_CONTEXT('part definition',#7045,'design');
#6994=PRODUCT_DEFINITION('Pipe section (1)','Pipe section (1)',
#7014,#6983);
#7014=PRODUCT_DEFINITION_FORMATION('',$,#7057);
#7045=APPLICATION_CONTEXT(
'Core Data for Automotive Mechanical Design Process');
#7046=PRODUCT_CONTEXT('part definition',#7045,'mechanical');
#7057=PRODUCT('Pipe section (1)','Pipe section (1)',
'Pipe section (1)',(#7046));
#7116=COLOUR_RGB('Sky Blue',0.24,0.69,0.87);
#7117=FILL_AREA_STYLE_COLOUR('',#7116);
#7118=FILL_AREA_STYLE('',(#7117));
#7119=SURFACE_STYLE_FILL_AREA(#7118);
#7120=SURFACE_SIDE_STYLE('',(#7119));
#7121=SURFACE_STYLE_USAGE(.BOTH.,#7120);
#7122=PRESENTATION_STYLE_ASSIGNMENT((#7121));
ENDSEC;
END-ISO-10303-21;
